ISO-10303-21;
HEADER;
/* Generated by software containing ST-Developer
 * from STEP Tools, Inc. (www.steptools.com) 
 */

FILE_DESCRIPTION(
/* description */ ('Flange-mounted spindle'),
/* implementation_level */ '2;1');

FILE_NAME(
/* name */ 'Cap Screw - M8x30.step',
/* time_stamp */ '2026-10-27T10:49:51-07:00',
/* author */ (''),
/* organization */ (''),
/* preprocessor_version */ 'ST-DEVELOPER v20.2',
/* originating_system */ 'Autodesk Translation Framework v15.17.0.0',
/* authorisation */ '');

FILE_SCHEMA (('AUTOMOTIVE_DESIGN { 1 0 10303 214 3 1 1 }'));
ENDSEC;

DATA;
#10=MECHANICAL_DESIGN_GEOMETRIC_PRESENTATION_REPRESENTATION('',(#350),#11764);
#266=CONICAL_SURFACE('',#6651,0.625,0.785398163397448);
#267=CONICAL_SURFACE('',#6655,0.635,0.785398163397449);
#268=CONICAL_SURFACE('',#6659,0.41,0.463647609000806);
#269=CONICAL_SURFACE('',#6663,0.36,0.785398163397448);
#279=ORIENTED_CLOSED_SHELL('',*,#6144,.F.);
#282=BREP_WITH_VOIDS('Body1',#6143,(#279));
#295=SHAPE_REPRESENTATION_RELATIONSHIP('SRR','None',#11892,#322);
#322=ADVANCED_BREP_SHAPE_REPRESENTATION('',(#282),#11747);
#350=STYLED_ITEM('',(#12106),#282);
#451=FACE_BOUND('',#1188,.T.);
#568=PLANE('',#6649);
#569=PLANE('',#6657);
#570=PLANE('',#6665);
#571=PLANE('',#6666);
#572=PLANE('',#6667);
#573=PLANE('',#6668);
#574=PLANE('',#6669);
#575=PLANE('',#6670);
#576=PLANE('',#6671);
#577=PLANE('',#6672);
#578=PLANE('',#6673);
#778=FACE_OUTER_BOUND('',#1183,.T.);
#779=FACE_OUTER_BOUND('',#1184,.T.);
#780=FACE_OUTER_BOUND('',#1185,.T.);
#781=FACE_OUTER_BOUND('',#1186,.T.);
#782=FACE_OUTER_BOUND('',#1187,.T.);
#783=FACE_OUTER_BOUND('',#1189,.T.);
#784=FACE_OUTER_BOUND('',#1190,.T.);
#785=FACE_OUTER_BOUND('',#1191,.T.);
#786=FACE_OUTER_BOUND('',#1192,.T.);
#787=FACE_OUTER_BOUND('',#1193,.T.);
#788=FACE_OUTER_BOUND('',#1194,.T.);
#789=FACE_OUTER_BOUND('',#1195,.T.);
#790=FACE_OUTER_BOUND('',#1196,.T.);
#791=FACE_OUTER_BOUND('',#1197,.T.);
#792=FACE_OUTER_BOUND('',#1198,.T.);
#793=FACE_OUTER_BOUND('',#1199,.T.);
#794=FACE_OUTER_BOUND('',#1200,.T.);
#1183=EDGE_LOOP('',(#4463));
#1184=EDGE_LOOP('',(#4464,#4465,#4466,#4467));
#1185=EDGE_LOOP('',(#4468,#4469,#4470,#4471));
#1186=EDGE_LOOP('',(#4472,#4473,#4474,#4475));
#1187=EDGE_LOOP('',(#4476));
#1188=EDGE_LOOP('',(#4477));
#1189=EDGE_LOOP('',(#4478,#4479,#4480,#4481));
#1190=EDGE_LOOP('',(#4482,#4483,#4484,#4485));
#1191=EDGE_LOOP('',(#4486,#4487,#4488,#4489));
#1192=EDGE_LOOP('',(#4490));
#1193=EDGE_LOOP('',(#4491,#4492,#4493,#4494));
#1194=EDGE_LOOP('',(#4495,#4496,#4497,#4498));
#1195=EDGE_LOOP('',(#4499,#4500,#4501,#4502));
#1196=EDGE_LOOP('',(#4503,#4504,#4505,#4506));
#1197=EDGE_LOOP('',(#4507,#4508,#4509,#4510));
#1198=EDGE_LOOP('',(#4511,#4512,#4513,#4514));
#1199=EDGE_LOOP('',(#4515,#4516,#4517,#4518,#4519,#4520));
#1200=EDGE_LOOP('',(#4521,#4522,#4523,#4524,#4525,#4526));
#1615=LINE('',#10051,#2037);
#1616=LINE('',#10055,#2038);
#1617=LINE('',#10059,#2039);
#1618=LINE('',#10066,#2040);
#1619=LINE('',#10070,#2041);
#1620=LINE('',#10074,#2042);
#1621=LINE('',#10079,#2043);
#1622=LINE('',#10081,#2044);
#1623=LINE('',#10083,#2045);
#1624=LINE('',#10084,#2046);
#1625=LINE('',#10087,#2047);
#1626=LINE('',#10089,#2048);
#1627=LINE('',#10090,#2049);
#1628=LINE('',#10093,#2050);
#1629=LINE('',#10095,#2051);
#1630=LINE('',#10096,#2052);
#1631=LINE('',#10099,#2053);
#1632=LINE('',#10101,#2054);
#1633=LINE('',#10102,#2055);
#1634=LINE('',#10105,#2056);
#1635=LINE('',#10107,#2057);
#1636=LINE('',#10108,#2058);
#1637=LINE('',#10110,#2059);
#1638=LINE('',#10111,#2060);
#2037=VECTOR('',#7732,0.625);
#2038=VECTOR('',#7737,0.65);
#2039=VECTOR('',#7742,0.635);
#2040=VECTOR('',#7751,0.41);
#2041=VECTOR('',#7756,0.4);
#2042=VECTOR('',#7761,0.36);
#2043=VECTOR('',#7766,1.);
#2044=VECTOR('',#7767,1.);
#2045=VECTOR('',#7768,1.);
#2046=VECTOR('',#7769,1.);
#2047=VECTOR('',#7772,1.);
#2048=VECTOR('',#7773,1.);
#2049=VECTOR('',#7774,1.);
#2050=VECTOR('',#7777,1.);
#2051=VECTOR('',#7778,1.);
#2052=VECTOR('',#7779,1.);
#2053=VECTOR('',#7782,1.);
#2054=VECTOR('',#7783,1.);
#2055=VECTOR('',#7784,1.);
#2056=VECTOR('',#7787,1.);
#2057=VECTOR('',#7788,1.);
#2058=VECTOR('',#7789,1.);
#2059=VECTOR('',#7792,1.);
#2060=VECTOR('',#7793,1.);
#2392=CIRCLE('',#6650,0.6);
#2393=CIRCLE('',#6652,0.65);
#2394=CIRCLE('',#6654,0.65);
#2395=CIRCLE('',#6656,0.62);
#2396=CIRCLE('',#6658,0.42);
#2397=CIRCLE('',#6660,0.3933);
#2398=CIRCLE('',#6662,0.3933);
#2399=CIRCLE('',#6664,0.32);
#2808=VERTEX_POINT('',#10046);
#2809=VERTEX_POINT('',#10049);
#2810=VERTEX_POINT('',#10053);
#2811=VERTEX_POINT('',#10057);
#2812=VERTEX_POINT('',#10061);
#2813=VERTEX_POINT('',#10064);
#2814=VERTEX_POINT('',#10068);
#2815=VERTEX_POINT('',#10072);
#2816=VERTEX_POINT('',#10077);
#2817=VERTEX_POINT('',#10078);
#2818=VERTEX_POINT('',#10080);
#2819=VERTEX_POINT('',#10082);
#2820=VERTEX_POINT('',#10086);
#2821=VERTEX_POINT('',#10088);
#2822=VERTEX_POINT('',#10092);
#2823=VERTEX_POINT('',#10094);
#2824=VERTEX_POINT('',#10098);
#2825=VERTEX_POINT('',#10100);
#2826=VERTEX_POINT('',#10104);
#2827=VERTEX_POINT('',#10106);
#3424=EDGE_CURVE('',#2808,#2808,#2392,.T.);
#3425=EDGE_CURVE('',#2809,#2809,#2393,.T.);
#3426=EDGE_CURVE('',#2809,#2808,#1615,.T.);
#3427=EDGE_CURVE('',#2810,#2810,#2394,.T.);
#3428=EDGE_CURVE('',#2810,#2809,#1616,.T.);
#3429=EDGE_CURVE('',#2811,#2811,#2395,.T.);
#3430=EDGE_CURVE('',#2811,#2810,#1617,.T.);
#3431=EDGE_CURVE('',#2812,#2812,#2396,.T.);
#3432=EDGE_CURVE('',#2813,#2813,#2397,.F.);
#3433=EDGE_CURVE('',#2813,#2812,#1618,.T.);
#3434=EDGE_CURVE('',#2814,#2814,#2398,.F.);
#3435=EDGE_CURVE('',#2814,#2813,#1619,.T.);
#3436=EDGE_CURVE('',#2815,#2815,#2399,.T.);
#3437=EDGE_CURVE('',#2815,#2814,#1620,.T.);
#3438=EDGE_CURVE('',#2816,#2817,#1621,.T.);
#3439=EDGE_CURVE('',#2817,#2818,#1622,.T.);
#3440=EDGE_CURVE('',#2818,#2819,#1623,.T.);
#3441=EDGE_CURVE('',#2816,#2819,#1624,.T.);
#3442=EDGE_CURVE('',#2817,#2820,#1625,.T.);
#3443=EDGE_CURVE('',#2820,#2821,#1626,.T.);
#3444=EDGE_CURVE('',#2821,#2818,#1627,.T.);
#3445=EDGE_CURVE('',#2820,#2822,#1628,.T.);
#3446=EDGE_CURVE('',#2822,#2823,#1629,.T.);
#3447=EDGE_CURVE('',#2823,#2821,#1630,.T.);
#3448=EDGE_CURVE('',#2822,#2824,#1631,.T.);
#3449=EDGE_CURVE('',#2824,#2825,#1632,.T.);
#3450=EDGE_CURVE('',#2825,#2823,#1633,.T.);
#3451=EDGE_CURVE('',#2824,#2826,#1634,.T.);
#3452=EDGE_CURVE('',#2826,#2827,#1635,.T.);
#3453=EDGE_CURVE('',#2827,#2825,#1636,.T.);
#3454=EDGE_CURVE('',#2826,#2816,#1637,.T.);
#3455=EDGE_CURVE('',#2819,#2827,#1638,.T.);
#4463=ORIENTED_EDGE('',*,*,#3424,.F.);
#4464=ORIENTED_EDGE('',*,*,#3425,.F.);
#4465=ORIENTED_EDGE('',*,*,#3426,.T.);
#4466=ORIENTED_EDGE('',*,*,#3424,.T.);
#4467=ORIENTED_EDGE('',*,*,#3426,.F.);
#4468=ORIENTED_EDGE('',*,*,#3427,.F.);
#4469=ORIENTED_EDGE('',*,*,#3428,.T.);
#4470=ORIENTED_EDGE('',*,*,#3425,.T.);
#4471=ORIENTED_EDGE('',*,*,#3428,.F.);
#4472=ORIENTED_EDGE('',*,*,#3429,.F.);
#4473=ORIENTED_EDGE('',*,*,#3430,.T.);
#4474=ORIENTED_EDGE('',*,*,#3427,.T.);
#4475=ORIENTED_EDGE('',*,*,#3430,.F.);
#4476=ORIENTED_EDGE('',*,*,#3429,.T.);
#4477=ORIENTED_EDGE('',*,*,#3431,.F.);
#4478=ORIENTED_EDGE('',*,*,#3432,.F.);
#4479=ORIENTED_EDGE('',*,*,#3433,.T.);
#4480=ORIENTED_EDGE('',*,*,#3431,.T.);
#4481=ORIENTED_EDGE('',*,*,#3433,.F.);
#4482=ORIENTED_EDGE('',*,*,#3434,.F.);
#4483=ORIENTED_EDGE('',*,*,#3435,.T.);
#4484=ORIENTED_EDGE('',*,*,#3432,.T.);
#4485=ORIENTED_EDGE('',*,*,#3435,.F.);
#4486=ORIENTED_EDGE('',*,*,#3436,.F.);
#4487=ORIENTED_EDGE('',*,*,#3437,.T.);
#4488=ORIENTED_EDGE('',*,*,#3434,.T.);
#4489=ORIENTED_EDGE('',*,*,#3437,.F.);
#4490=ORIENTED_EDGE('',*,*,#3436,.T.);
#4491=ORIENTED_EDGE('',*,*,#3438,.T.);
#4492=ORIENTED_EDGE('',*,*,#3439,.T.);
#4493=ORIENTED_EDGE('',*,*,#3440,.T.);
#4494=ORIENTED_EDGE('',*,*,#3441,.F.);
#4495=ORIENTED_EDGE('',*,*,#3442,.T.);
#4496=ORIENTED_EDGE('',*,*,#3443,.T.);
#4497=ORIENTED_EDGE('',*,*,#3444,.T.);
#4498=ORIENTED_EDGE('',*,*,#3439,.F.);
#4499=ORIENTED_EDGE('',*,*,#3445,.T.);
#4500=ORIENTED_EDGE('',*,*,#3446,.T.);
#4501=ORIENTED_EDGE('',*,*,#3447,.T.);
#4502=ORIENTED_EDGE('',*,*,#3443,.F.);
#4503=ORIENTED_EDGE('',*,*,#3448,.T.);
#4504=ORIENTED_EDGE('',*,*,#3449,.T.);
#4505=ORIENTED_EDGE('',*,*,#3450,.T.);
#4506=ORIENTED_EDGE('',*,*,#3446,.F.);
#4507=ORIENTED_EDGE('',*,*,#3451,.T.);
#4508=ORIENTED_EDGE('',*,*,#3452,.T.);
#4509=ORIENTED_EDGE('',*,*,#3453,.T.);
#4510=ORIENTED_EDGE('',*,*,#3449,.F.);
#4511=ORIENTED_EDGE('',*,*,#3454,.T.);
#4512=ORIENTED_EDGE('',*,*,#3441,.T.);
#4513=ORIENTED_EDGE('',*,*,#3455,.T.);
#4514=ORIENTED_EDGE('',*,*,#3452,.F.);
#4515=ORIENTED_EDGE('',*,*,#3454,.F.);
#4516=ORIENTED_EDGE('',*,*,#3451,.F.);
#4517=ORIENTED_EDGE('',*,*,#3448,.F.);
#4518=ORIENTED_EDGE('',*,*,#3445,.F.);
#4519=ORIENTED_EDGE('',*,*,#3442,.F.);
#4520=ORIENTED_EDGE('',*,*,#3438,.F.);
#4521=ORIENTED_EDGE('',*,*,#3455,.F.);
#4522=ORIENTED_EDGE('',*,*,#3440,.F.);
#4523=ORIENTED_EDGE('',*,*,#3444,.F.);
#4524=ORIENTED_EDGE('',*,*,#3447,.F.);
#4525=ORIENTED_EDGE('',*,*,#3450,.F.);
#4526=ORIENTED_EDGE('',*,*,#3453,.F.);
#5662=CYLINDRICAL_SURFACE('',#6653,0.65);
#5663=CYLINDRICAL_SURFACE('',#6661,0.3933);
#5889=ADVANCED_FACE('',(#778),#568,.T.);
#5890=ADVANCED_FACE('',(#779),#266,.T.);
#5891=ADVANCED_FACE('',(#780),#5662,.T.);
#5892=ADVANCED_FACE('',(#781),#267,.T.);
#5893=ADVANCED_FACE('',(#782,#451),#569,.T.);
#5894=ADVANCED_FACE('',(#783),#268,.T.);
#5895=ADVANCED_FACE('',(#784),#5663,.T.);
#5896=ADVANCED_FACE('',(#785),#269,.T.);
#5897=ADVANCED_FACE('',(#786),#570,.T.);
#5898=ADVANCED_FACE('',(#787),#571,.F.);
#5899=ADVANCED_FACE('',(#788),#572,.F.);
#5900=ADVANCED_FACE('',(#789),#573,.F.);
#5901=ADVANCED_FACE('',(#790),#574,.F.);
#5902=ADVANCED_FACE('',(#791),#575,.F.);
#5903=ADVANCED_FACE('',(#792),#576,.F.);
#5904=ADVANCED_FACE('',(#793),#577,.F.);
#5905=ADVANCED_FACE('',(#794),#578,.F.);
#6143=CLOSED_SHELL('',(#5889,#5890,#5891,#5892,#5893,#5894,#5895,#5896,
#5897));
#6144=CLOSED_SHELL('',(#5898,#5899,#5900,#5901,#5902,#5903,#5904,#5905));
#6648=AXIS2_PLACEMENT_3D('',#10044,#7722,#7723);
#6649=AXIS2_PLACEMENT_3D('',#10045,#7724,#7725);
#6650=AXIS2_PLACEMENT_3D('',#10047,#7726,#7727);
#6651=AXIS2_PLACEMENT_3D('',#10048,#7728,#7729);
#6652=AXIS2_PLACEMENT_3D('',#10050,#7730,#7731);
#6653=AXIS2_PLACEMENT_3D('',#10052,#7733,#7734);
#6654=AXIS2_PLACEMENT_3D('',#10054,#7735,#7736);
#6655=AXIS2_PLACEMENT_3D('',#10056,#7738,#7739);
#6656=AXIS2_PLACEMENT_3D('',#10058,#7740,#7741);
#6657=AXIS2_PLACEMENT_3D('',#10060,#7743,#7744);
#6658=AXIS2_PLACEMENT_3D('',#10062,#7745,#7746);
#6659=AXIS2_PLACEMENT_3D('',#10063,#7747,#7748);
#6660=AXIS2_PLACEMENT_3D('',#10065,#7749,#7750);
#6661=AXIS2_PLACEMENT_3D('',#10067,#7752,#7753);
#6662=AXIS2_PLACEMENT_3D('',#10069,#7754,#7755);
#6663=AXIS2_PLACEMENT_3D('',#10071,#7757,#7758);
#6664=AXIS2_PLACEMENT_3D('',#10073,#7759,#7760);
#6665=AXIS2_PLACEMENT_3D('',#10075,#7762,#7763);
#6666=AXIS2_PLACEMENT_3D('',#10076,#7764,#7765);
#6667=AXIS2_PLACEMENT_3D('',#10085,#7770,#7771);
#6668=AXIS2_PLACEMENT_3D('',#10091,#7775,#7776);
#6669=AXIS2_PLACEMENT_3D('',#10097,#7780,#7781);
#6670=AXIS2_PLACEMENT_3D('',#10103,#7785,#7786);
#6671=AXIS2_PLACEMENT_3D('',#10109,#7790,#7791);
#6672=AXIS2_PLACEMENT_3D('',#10112,#7794,#7795);
#6673=AXIS2_PLACEMENT_3D('',#10113,#7796,#7797);
#7722=DIRECTION('axis',(0.,0.,1.));
#7723=DIRECTION('refdir',(1.,0.,0.));
#7724=DIRECTION('center_axis',(0.,1.,0.));
#7725=DIRECTION('ref_axis',(0.,0.,1.));
#7726=DIRECTION('center_axis',(0.,-1.,0.));
#7727=DIRECTION('ref_axis',(1.,0.,0.));
#7728=DIRECTION('center_axis',(0.,-1.,0.));
#7729=DIRECTION('ref_axis',(1.,0.,0.));
#7730=DIRECTION('center_axis',(0.,-1.,0.));
#7731=DIRECTION('ref_axis',(1.,0.,0.));
#7732=DIRECTION('',(0.707106781186548,0.707106781186547,8.65956056235493E-17));
#7733=DIRECTION('center_axis',(0.,-1.,0.));
#7734=DIRECTION('ref_axis',(1.,0.,0.));
#7735=DIRECTION('center_axis',(0.,-1.,0.));
#7736=DIRECTION('ref_axis',(1.,0.,0.));
#7737=DIRECTION('',(0.,1.,0.));
#7738=DIRECTION('center_axis',(0.,1.,0.));
#7739=DIRECTION('ref_axis',(1.,0.,0.));
#7740=DIRECTION('center_axis',(0.,-1.,0.));
#7741=DIRECTION('ref_axis',(1.,0.,0.));
#7742=DIRECTION('',(-0.707106781186548,0.707106781186547,-8.65956056235494E-17));
#7743=DIRECTION('center_axis',(0.,-1.,0.));
#7744=DIRECTION('ref_axis',(0.,0.,-1.));
#7745=DIRECTION('center_axis',(0.,-1.,0.));
#7746=DIRECTION('ref_axis',(1.,0.,0.));
#7747=DIRECTION('center_axis',(0.,1.,0.));
#7748=DIRECTION('ref_axis',(1.,0.,0.));
#7749=DIRECTION('center_axis',(0.,1.,0.));
#7750=DIRECTION('ref_axis',(1.,0.,0.));
#7751=DIRECTION('',(-0.447213595499958,0.894427190999916,-5.47678698264203E-17));
#7752=DIRECTION('center_axis',(0.,-1.,0.));
#7753=DIRECTION('ref_axis',(1.,0.,0.));
#7754=DIRECTION('center_axis',(0.,1.,0.));
#7755=DIRECTION('ref_axis',(1.,0.,0.));
#7756=DIRECTION('',(0.,1.,0.));
#7757=DIRECTION('center_axis',(0.,1.,0.));
#7758=DIRECTION('ref_axis',(1.,0.,0.));
#7759=DIRECTION('center_axis',(0.,-1.,0.));
#7760=DIRECTION('ref_axis',(1.,0.,0.));
#7761=DIRECTION('',(-0.707106781186547,0.707106781186548,-8.65956056235493E-17));
#7762=DIRECTION('center_axis',(0.,-1.,0.));
#7763=DIRECTION('ref_axis',(0.,0.,-1.));
#7764=DIRECTION('center_axis',(0.866025403784439,0.,-0.5));
#7765=DIRECTION('ref_axis',(0.5,0.,0.866025403784439));
#7766=DIRECTION('',(-0.5,0.,-0.866025403784439));
#7767=DIRECTION('',(0.,-1.,0.));
#7768=DIRECTION('',(0.5,0.,0.866025403784439));
#7769=DIRECTION('',(0.,-1.,0.));
#7770=DIRECTION('center_axis',(1.60246890531964E-16,0.,-1.));
#7771=DIRECTION('ref_axis',(1.,0.,1.60246890531964E-16));
#7772=DIRECTION('',(-1.,0.,-1.60246890531964E-16));
#7773=DIRECTION('',(0.,-1.,0.));
#7774=DIRECTION('',(1.,0.,1.60246890531964E-16));
#7775=DIRECTION('center_axis',(-0.866025403784439,0.,-0.5));
#7776=DIRECTION('ref_axis',(0.5,0.,-0.866025403784439));
#7777=DIRECTION('',(-0.5,0.,0.866025403784439));
#7778=DIRECTION('',(0.,-1.,0.));
#7779=DIRECTION('',(0.5,0.,-0.866025403784439));
#7780=DIRECTION('center_axis',(-0.866025403784439,0.,0.5));
#7781=DIRECTION('ref_axis',(-0.5,0.,-0.866025403784439));
#7782=DIRECTION('',(0.5,0.,0.866025403784439));
#7783=DIRECTION('',(0.,-1.,0.));
#7784=DIRECTION('',(-0.5,0.,-0.866025403784439));
#7785=DIRECTION('center_axis',(-1.60246890531964E-16,0.,1.));
#7786=DIRECTION('ref_axis',(-1.,0.,-1.60246890531964E-16));
#7787=DIRECTION('',(1.,0.,1.60246890531964E-16));
#7788=DIRECTION('',(0.,-1.,0.));
#7789=DIRECTION('',(-1.,0.,-1.60246890531964E-16));
#7790=DIRECTION('center_axis',(0.866025403784439,0.,0.5));
#7791=DIRECTION('ref_axis',(-0.5,0.,0.866025403784439));
#7792=DIRECTION('',(0.5,0.,-0.866025403784439));
#7793=DIRECTION('',(-0.5,0.,0.866025403784439));
#7794=DIRECTION('center_axis',(0.,1.,0.));
#7795=DIRECTION('ref_axis',(1.,0.,0.));
#7796=DIRECTION('center_axis',(0.,-1.,0.));
#7797=DIRECTION('ref_axis',(0.,0.,-1.));
#10044=CARTESIAN_POINT('',(0.,0.,0.));
#10045=CARTESIAN_POINT('Origin',(0.6,0.8,0.));
#10046=CARTESIAN_POINT('',(-0.6,0.8,-7.34788079488412E-17));
#10047=CARTESIAN_POINT('Origin',(0.,0.8,0.));
#10048=CARTESIAN_POINT('Origin',(0.,0.775,0.));
#10049=CARTESIAN_POINT('',(-0.65,0.75,-7.9602041944578E-17));
#10050=CARTESIAN_POINT('Origin',(0.,0.75,0.));
#10051=CARTESIAN_POINT('',(-0.625,0.775,-7.65404249467096E-17));
#10052=CARTESIAN_POINT('Origin',(0.,0.39,0.));
#10053=CARTESIAN_POINT('',(-0.65,0.0299999999999998,-7.9602041944578E-17));
#10054=CARTESIAN_POINT('Origin',(0.,0.0299999999999998,0.));
#10055=CARTESIAN_POINT('',(-0.65,0.39,-7.9602041944578E-17));
#10056=CARTESIAN_POINT('Origin',(0.,0.0150000000000001,0.));
#10057=CARTESIAN_POINT('',(-0.62,5.89805981832114E-17,-7.59281015471359E-17));
#10058=CARTESIAN_POINT('Origin',(0.,0.,0.));
#10059=CARTESIAN_POINT('',(-0.635,0.0150000000000001,-7.77650717458569E-17));
#10060=CARTESIAN_POINT('Origin',(0.42,0.,0.));
#10061=CARTESIAN_POINT('',(-0.42,-3.46944695195361E-18,-5.14351655641888E-17));
#10062=CARTESIAN_POINT('Origin',(0.,0.,0.));
#10063=CARTESIAN_POINT('Origin',(0.,-0.02,0.));
#10064=CARTESIAN_POINT('',(-0.3933,-0.0534000000000001,4.81653586104654E-17));
#10065=CARTESIAN_POINT('Origin',(0.,-0.0534000000000001,0.));
#10066=CARTESIAN_POINT('',(-0.41,-0.02,-5.02105187650415E-17));
#10067=CARTESIAN_POINT('Origin',(0.,-1.48,0.));
#10068=CARTESIAN_POINT('',(-0.3933,-2.9267,4.81653586104654E-17));
#10069=CARTESIAN_POINT('Origin',(0.,-2.9267,0.));
#10070=CARTESIAN_POINT('',(-0.3933,-1.48,-4.81653586104654E-17));
#10071=CARTESIAN_POINT('Origin',(0.,-2.96,0.));
#10072=CARTESIAN_POINT('',(-0.32,-3.,-3.91886975727153E-17));
#10073=CARTESIAN_POINT('Origin',(0.,-3.,0.));
#10074=CARTESIAN_POINT('',(-0.36,-2.96,-4.40872847693047E-17));
#10075=CARTESIAN_POINT('Origin',(0.,-3.,0.));
#10076=CARTESIAN_POINT('Origin',(0.173205080756888,-0.8,-0.3));
#10077=CARTESIAN_POINT('',(0.346410161513775,-0.8,0.));
#10078=CARTESIAN_POINT('',(0.173205080756888,-0.8,-0.3));
#10079=CARTESIAN_POINT('',(0.346410161513775,-0.8,0.));
#10080=CARTESIAN_POINT('',(0.173205080756888,-1.28,-0.3));
#10081=CARTESIAN_POINT('',(0.173205080756888,-0.8,-0.3));
#10082=CARTESIAN_POINT('',(0.346410161513775,-1.28,0.));
#10083=CARTESIAN_POINT('',(0.346410161513775,-1.28,0.));
#10084=CARTESIAN_POINT('',(0.346410161513775,-0.8,0.));
#10085=CARTESIAN_POINT('Origin',(-0.173205080756888,-0.8,-0.3));
#10086=CARTESIAN_POINT('',(-0.173205080756888,-0.8,-0.3));
#10087=CARTESIAN_POINT('',(0.173205080756888,-0.8,-0.3));
#10088=CARTESIAN_POINT('',(-0.173205080756888,-1.28,-0.3));
#10089=CARTESIAN_POINT('',(-0.173205080756888,-0.8,-0.3));
#10090=CARTESIAN_POINT('',(0.173205080756888,-1.28,-0.3));
#10091=CARTESIAN_POINT('Origin',(-0.346410161513775,-0.8,-5.55111512312578E-17));
#10092=CARTESIAN_POINT('',(-0.346410161513775,-0.8,-4.24230095489963E-17));
#10093=CARTESIAN_POINT('',(-0.173205080756888,-0.8,-0.3));
#10094=CARTESIAN_POINT('',(-0.346410161513775,-1.28,-5.55111512312578E-17));
#10095=CARTESIAN_POINT('',(-0.346410161513775,-0.8,-4.24230095489963E-17));
#10096=CARTESIAN_POINT('',(-0.173205080756888,-1.28,-0.3));
#10097=CARTESIAN_POINT('Origin',(-0.173205080756888,-0.8,0.3));
#10098=CARTESIAN_POINT('',(-0.173205080756888,-0.8,0.3));
#10099=CARTESIAN_POINT('',(-0.346410161513775,-0.8,-4.24230095489963E-17));
#10100=CARTESIAN_POINT('',(-0.173205080756888,-1.28,0.3));
#10101=CARTESIAN_POINT('',(-0.173205080756888,-0.8,0.3));
#10102=CARTESIAN_POINT('',(-0.346410161513775,-1.28,-4.24230095489963E-17));
#10103=CARTESIAN_POINT('Origin',(0.173205080756888,-0.8,0.3));
#10104=CARTESIAN_POINT('',(0.173205080756888,-0.8,0.3));
#10105=CARTESIAN_POINT('',(-0.173205080756888,-0.8,0.3));
#10106=CARTESIAN_POINT('',(0.173205080756888,-1.28,0.3));
#10107=CARTESIAN_POINT('',(0.173205080756888,-0.8,0.3));
#10108=CARTESIAN_POINT('',(-0.173205080756888,-1.28,0.3));
#10109=CARTESIAN_POINT('Origin',(0.346410161513775,-0.8,0.));
#10110=CARTESIAN_POINT('',(0.173205080756888,-0.8,0.3));
#10111=CARTESIAN_POINT('',(0.173205080756888,-1.28,0.3));
#10112=CARTESIAN_POINT('Origin',(0.,-0.8,-5.55111512312578E-17));
#10113=CARTESIAN_POINT('Origin',(0.,-1.28,-5.55111512312578E-17));
#11715=UNCERTAINTY_MEASURE_WITH_UNIT(LENGTH_MEASURE(0.001),#11765,
'DISTANCE_ACCURACY_VALUE',
'Maximum model space distance between geometric entities at asserted c
onnectivities');
#11732=UNCERTAINTY_MEASURE_WITH_UNIT(LENGTH_MEASURE(0.001),#11765,
'DISTANCE_ACCURACY_VALUE',
'Maximum model space distance between geometric entities at asserted c
onnectivities');
#11747=(
GEOMETRIC_REPRESENTATION_CONTEXT(3)
GLOBAL_UNCERTAINTY_ASSIGNED_CONTEXT((#11715))
GLOBAL_UNIT_ASSIGNED_CONTEXT((#11765,#11767,#11768))
REPRESENTATION_CONTEXT('','3D')
);
#11764=(
GEOMETRIC_REPRESENTATION_CONTEXT(3)
GLOBAL_UNCERTAINTY_ASSIGNED_CONTEXT((#11732))
GLOBAL_UNIT_ASSIGNED_CONTEXT((#11765,#11767,#11768))
REPRESENTATION_CONTEXT('','3D')
);
#11765=(
LENGTH_UNIT()
NAMED_UNIT(*)
SI_UNIT(.CENTI.,.METRE.)
);
#11767=(
NAMED_UNIT(*)
PLANE_ANGLE_UNIT()
SI_UNIT($,.RADIAN.)
);
#11768=(
NAMED_UNIT(*)
SI_UNIT($,.STERADIAN.)
SOLID_ANGLE_UNIT()
);
#11783=SHAPE_DEFINITION_REPRESENTATION(#11816,#11892);
#11816=PRODUCT_DEFINITION_SHAPE('',$,#11924);
#11892=SHAPE_REPRESENTATION('',(#6648),#11747);
#11909=PRODUCT_DEFINITION_CONTEXT('part definition',#12004,'design');
#11924=PRODUCT_DEFINITION('Cap Screw - M8x30','Cap Screw - M8x30',#11955,
#11909);
#11955=PRODUCT_DEFINITION_FORMATION('',$,#12020);
#12004=APPLICATION_CONTEXT(
'Core Data for Automotive Mechanical Design Process');
#12005=PRODUCT_CONTEXT('part definition',#12004,'mechanical');
#12020=PRODUCT('Cap Screw - M8x30','Cap Screw - M8x30',
'Cap Screw - M8x30',(#12005));
#12100=COLOUR_RGB('Black',0.12,0.14,0.17);
#12101=FILL_AREA_STYLE_COLOUR('',#12100);
#12102=FILL_AREA_STYLE('',(#12101));
#12103=SURFACE_STYLE_FILL_AREA(#12102);
#12104=SURFACE_SIDE_STYLE('',(#12103));
#12105=SURFACE_STYLE_USAGE(.BOTH.,#12104);
#12106=PRESENTATION_STYLE_ASSIGNMENT((#12105));
ENDSEC;
END-ISO-10303-21;
